ISO-10303-21;
HEADER;
/* Generated by software containing ST-Developer
 * from STEP Tools, Inc. (www.steptools.com) 
 */

FILE_DESCRIPTION(
/* description */ ('Hinged panel with latch'),
/* implementation_level */ '2;1');

FILE_NAME(
/* name */ 'Flat Washer - M5.step',
/* time_stamp */ '2026-10-27T20:36:01-07:00',
/* author */ (''),
/* organization */ (''),
/* preprocessor_version */ 'ST-DEVELOPER v20.2',
/* originating_system */ 'Autodesk Translation Framework v15.17.0.0',
/* authorisation */ '');

FILE_SCHEMA (('AUTOMOTIVE_DESIGN { 1 0 10303 214 3 1 1 }'));
ENDSEC;

DATA;
#10=MECHANICAL_DESIGN_GEOMETRIC_PRESENTATION_REPRESENTATION('',(#308),#6743);
#251=CONICAL_SURFACE('',#4252,0.275,0.785398163397449);
#276=SHAPE_REPRESENTATION_RELATIONSHIP('SRR','None',#6852,#292);
#292=ADVANCED_BREP_SHAPE_REPRESENTATION('',(#322),#6738);
#308=STYLED_ITEM('',(#7010),#322);
#322=MANIFOLD_SOLID_BREP('Body1',#3812);
#365=FACE_BOUND('',#938,.T.);
#366=FACE_BOUND('',#941,.T.);
#496=PLANE('',#4257);
#497=PLANE('',#4261);
#689=FACE_OUTER_BOUND('',#935,.T.);
#690=FACE_OUTER_BOUND('',#936,.T.);
#691=FACE_OUTER_BOUND('',#937,.T.);
#692=FACE_OUTER_BOUND('',#939,.T.);
#693=FACE_OUTER_BOUND('',#940,.T.);
#935=EDGE_LOOP('',(#3396,#3397,#3398,#3399));
#936=EDGE_LOOP('',(#3400,#3401,#3402,#3403));
#937=EDGE_LOOP('',(#3404));
#938=EDGE_LOOP('',(#3405));
#939=EDGE_LOOP('',(#3406,#3407,#3408,#3409));
#940=EDGE_LOOP('',(#3410));
#941=EDGE_LOOP('',(#3411));
#1291=LINE('',#6458,#1649);
#1292=LINE('',#6462,#1650);
#1293=LINE('',#6469,#1651);
#1649=VECTOR('',#5193,0.275);
#1650=VECTOR('',#5198,0.265);
#1651=VECTOR('',#5207,0.5);
#1772=CIRCLE('',#4253,0.285);
#1773=CIRCLE('',#4254,0.265);
#1774=CIRCLE('',#4256,0.265);
#1775=CIRCLE('',#4258,0.5);
#1776=CIRCLE('',#4260,0.5);
#2056=VERTEX_POINT('',#6455);
#2057=VERTEX_POINT('',#6457);
#2058=VERTEX_POINT('',#6461);
#2059=VERTEX_POINT('',#6465);
#2060=VERTEX_POINT('',#6468);
#2510=EDGE_CURVE('',#2056,#2056,#1772,.T.);
#2511=EDGE_CURVE('',#2056,#2057,#1291,.T.);
#2512=EDGE_CURVE('',#2057,#2057,#1773,.T.);
#2513=EDGE_CURVE('',#2057,#2058,#1292,.T.);
#2514=EDGE_CURVE('',#2058,#2058,#1774,.T.);
#2515=EDGE_CURVE('',#2059,#2059,#1775,.T.);
#2516=EDGE_CURVE('',#2059,#2060,#1293,.T.);
#2517=EDGE_CURVE('',#2060,#2060,#1776,.T.);
#3396=ORIENTED_EDGE('',*,*,#2510,.T.);
#3397=ORIENTED_EDGE('',*,*,#2511,.T.);
#3398=ORIENTED_EDGE('',*,*,#2512,.T.);
#3399=ORIENTED_EDGE('',*,*,#2511,.F.);
#3400=ORIENTED_EDGE('',*,*,#2512,.F.);
#3401=ORIENTED_EDGE('',*,*,#2513,.T.);
#3402=ORIENTED_EDGE('',*,*,#2514,.T.);
#3403=ORIENTED_EDGE('',*,*,#2513,.F.);
#3404=ORIENTED_EDGE('',*,*,#2515,.T.);
#3405=ORIENTED_EDGE('',*,*,#2510,.F.);
#3406=ORIENTED_EDGE('',*,*,#2515,.F.);
#3407=ORIENTED_EDGE('',*,*,#2516,.T.);
#3408=ORIENTED_EDGE('',*,*,#2517,.T.);
#3409=ORIENTED_EDGE('',*,*,#2516,.F.);
#3410=ORIENTED_EDGE('',*,*,#2517,.F.);
#3411=ORIENTED_EDGE('',*,*,#2514,.F.);
#3586=CYLINDRICAL_SURFACE('',#4255,0.265);
#3587=CYLINDRICAL_SURFACE('',#4259,0.5);
#3758=ADVANCED_FACE('',(#689),#251,.F.);
#3759=ADVANCED_FACE('',(#690),#3586,.F.);
#3760=ADVANCED_FACE('',(#691,#365),#496,.T.);
#3761=ADVANCED_FACE('',(#692),#3587,.T.);
#3762=ADVANCED_FACE('',(#693,#366),#497,.F.);
#3812=CLOSED_SHELL('',(#3758,#3759,#3760,#3761,#3762));
#4251=AXIS2_PLACEMENT_3D('',#6453,#5187,#5188);
#4252=AXIS2_PLACEMENT_3D('',#6454,#5189,#5190);
#4253=AXIS2_PLACEMENT_3D('',#6456,#5191,#5192);
#4254=AXIS2_PLACEMENT_3D('',#6459,#5194,#5195);
#4255=AXIS2_PLACEMENT_3D('',#6460,#5196,#5197);
#4256=AXIS2_PLACEMENT_3D('',#6463,#5199,#5200);
#4257=AXIS2_PLACEMENT_3D('',#6464,#5201,#5202);
#4258=AXIS2_PLACEMENT_3D('',#6466,#5203,#5204);
#4259=AXIS2_PLACEMENT_3D('',#6467,#5205,#5206);
#4260=AXIS2_PLACEMENT_3D('',#6470,#5208,#5209);
#4261=AXIS2_PLACEMENT_3D('',#6471,#5210,#5211);
#5187=DIRECTION('axis',(0.,0.,1.));
#5188=DIRECTION('refdir',(1.,0.,0.));
#5189=DIRECTION('center_axis',(0.,1.,0.));
#5190=DIRECTION('ref_axis',(1.,0.,0.));
#5191=DIRECTION('center_axis',(0.,1.,0.));
#5192=DIRECTION('ref_axis',(1.,0.,0.));
#5193=DIRECTION('',(0.707106781186548,-0.707106781186547,-8.65956056235494E-17));
#5194=DIRECTION('center_axis',(0.,-1.,0.));
#5195=DIRECTION('ref_axis',(1.,0.,0.));
#5196=DIRECTION('center_axis',(0.,1.,0.));
#5197=DIRECTION('ref_axis',(1.,0.,0.));
#5198=DIRECTION('',(0.,-1.,0.));
#5199=DIRECTION('center_axis',(0.,-1.,0.));
#5200=DIRECTION('ref_axis',(1.,0.,0.));
#5201=DIRECTION('center_axis',(0.,1.,0.));
#5202=DIRECTION('ref_axis',(1.,0.,0.));
#5203=DIRECTION('center_axis',(0.,1.,0.));
#5204=DIRECTION('ref_axis',(1.,0.,0.));
#5205=DIRECTION('center_axis',(0.,1.,0.));
#5206=DIRECTION('ref_axis',(1.,0.,0.));
#5207=DIRECTION('',(0.,-1.,0.));
#5208=DIRECTION('center_axis',(0.,1.,0.));
#5209=DIRECTION('ref_axis',(1.,0.,0.));
#5210=DIRECTION('center_axis',(0.,1.,0.));
#5211=DIRECTION('ref_axis',(1.,0.,0.));
#6453=CARTESIAN_POINT('',(0.,0.,0.));
#6454=CARTESIAN_POINT('Origin',(0.,0.09,0.));
#6455=CARTESIAN_POINT('',(-0.285,0.1,3.49024337756996E-17));
#6456=CARTESIAN_POINT('Origin',(0.,0.1,0.));
#6457=CARTESIAN_POINT('',(-0.265,0.08,-3.24531401774049E-17));
#6458=CARTESIAN_POINT('',(-0.275,0.09,3.36777869765522E-17));
#6459=CARTESIAN_POINT('Origin',(0.,0.08,0.));
#6460=CARTESIAN_POINT('Origin',(0.,0.,0.));
#6461=CARTESIAN_POINT('',(-0.265,0.,3.24531401774049E-17));
#6462=CARTESIAN_POINT('',(-0.265,0.,3.24531401774049E-17));
#6463=CARTESIAN_POINT('Origin',(0.,0.,0.));
#6464=CARTESIAN_POINT('Origin',(0.,0.1,0.));
#6465=CARTESIAN_POINT('',(-0.5,0.1,6.12323399573677E-17));
#6466=CARTESIAN_POINT('Origin',(0.,0.1,0.));
#6467=CARTESIAN_POINT('Origin',(0.,0.,0.));
#6468=CARTESIAN_POINT('',(-0.5,0.,6.12323399573677E-17));
#6469=CARTESIAN_POINT('',(-0.5,0.,6.12323399573677E-17));
#6470=CARTESIAN_POINT('Origin',(0.,0.,0.));
#6471=CARTESIAN_POINT('Origin',(0.,0.,0.));
#6717=UNCERTAINTY_MEASURE_WITH_UNIT(LENGTH_MEASURE(0.001),#6744,
'DISTANCE_ACCURACY_VALUE',
'Maximum model space distance between geometric entities at asserted c
onnectivities');
#6722=UNCERTAINTY_MEASURE_WITH_UNIT(LENGTH_MEASURE(0.001),#6744,
'DISTANCE_ACCURACY_VALUE',
'Maximum model space distance between geometric entities at asserted c
onnectivities');
#6738=(
GEOMETRIC_REPRESENTATION_CONTEXT(3)
GLOBAL_UNCERTAINTY_ASSIGNED_CONTEXT((#6717))
GLOBAL_UNIT_ASSIGNED_CONTEXT((#6744,#6746,#6747))
REPRESENTATION_CONTEXT('','3D')
);
#6743=(
GEOMETRIC_REPRESENTATION_CONTEXT(3)
GLOBAL_UNCERTAINTY_ASSIGNED_CONTEXT((#6722))
GLOBAL_UNIT_ASSIGNED_CONTEXT((#6744,#6746,#6747))
REPRESENTATION_CONTEXT('','3D')
);
#6744=(
LENGTH_UNIT()
NAMED_UNIT(*)
SI_UNIT(.CENTI.,.METRE.)
);
#6746=(
NAMED_UNIT(*)
PLANE_ANGLE_UNIT()
SI_UNIT($,.RADIAN.)
);
#6747=(
NAMED_UNIT(*)
SI_UNIT($,.STERADIAN.)
SOLID_ANGLE_UNIT()
);
#6763=SHAPE_DEFINITION_REPRESENTATION(#6783,#6852);
#6783=PRODUCT_DEFINITION_SHAPE('',$,#6873);
#6852=SHAPE_REPRESENTATION('',(#4251),#6738);
#6857=PRODUCT_DEFINITION_CONTEXT('part definition',#6919,'design');
#6873=PRODUCT_DEFINITION('Flat Washer - M5','Flat Washer - M5',#6893,#6857);
#6893=PRODUCT_DEFINITION_FORMATION('',$,#6936);
#6919=APPLICATION_CONTEXT(
'Core Data for Automotive Mechanical Design Process');
#6920=PRODUCT_CONTEXT('part definition',#6919,'mechanical');
#6936=PRODUCT('Flat Washer - M5','Flat Washer - M5','Flat Washer - M5',
(#6920));
#7004=COLOUR_RGB('Black',0.12,0.14,0.17);
#7005=FILL_AREA_STYLE_COLOUR('',#7004);
#7006=FILL_AREA_STYLE('',(#7005));
#7007=SURFACE_STYLE_FILL_AREA(#7006);
#7008=SURFACE_SIDE_STYLE('',(#7007));
#7009=SURFACE_STYLE_USAGE(.BOTH.,#7008);
#7010=PRESENTATION_STYLE_ASSIGNMENT((#7009));
ENDSEC;
END-ISO-10303-21;
